ISO-10303-21;
HEADER;
/* Generated by software containing ST-Developer
 * from STEP Tools, Inc. (www.steptools.com) 
 */

FILE_DESCRIPTION(
/* description */ ('PAT-091'),
/* implementation_level */ '2;1');

FILE_NAME(
/* name */ 'M4 low-profile retaining screw (7).step',
/* time_stamp */ '2026-10-27T15:34:44-07:00',
/* author */ (''),
/* organization */ (''),
/* preprocessor_version */ 'ST-DEVELOPER v20.2',
/* originating_system */ 'Autodesk Translation Framework v15.17.0.0',
/* authorisation */ '');

FILE_SCHEMA (('AUTOMOTIVE_DESIGN { 1 0 10303 214 3 1 1 }'));
ENDSEC;

DATA;
#10=MECHANICAL_DESIGN_GEOMETRIC_PRESENTATION_REPRESENTATION('',(#1056),#25100);
#836=SHAPE_REPRESENTATION_RELATIONSHIP('SRR','None',#25603,#946);
#946=ADVANCED_BREP_SHAPE_REPRESENTATION('',(#1177),#25073);
#1056=STYLED_ITEM('',(#26198),#1177);
#1177=MANIFOLD_SOLID_BREP('Body1',#13336);
#1570=FACE_BOUND('',#3863,.T.);
#1983=PLANE('',#15943);
#1984=PLANE('',#15948);
#1985=PLANE('',#15951);
#2689=FACE_OUTER_BOUND('',#3862,.T.);
#2690=FACE_OUTER_BOUND('',#3864,.T.);
#2691=FACE_OUTER_BOUND('',#3865,.T.);
#2692=FACE_OUTER_BOUND('',#3866,.T.);
#2693=FACE_OUTER_BOUND('',#3867,.T.);
#3862=EDGE_LOOP('',(#11414));
#3863=EDGE_LOOP('',(#11415));
#3864=EDGE_LOOP('',(#11416,#11417,#11418,#11419));
#3865=EDGE_LOOP('',(#11420));
#3866=EDGE_LOOP('',(#11421,#11422,#11423,#11424));
#3867=EDGE_LOOP('',(#11425));
#4777=LINE('',#23859,#5517);
#4778=LINE('',#23863,#5518);
#5517=VECTOR('',#19847,0.350000000000001);
#5518=VECTOR('',#19852,0.199999999999999);
#6168=CIRCLE('',#15944,0.350000000000001);
#6169=CIRCLE('',#15945,0.199999999999999);
#6170=CIRCLE('',#15947,0.350000000000001);
#6171=CIRCLE('',#15950,0.199999999999999);
#7193=VERTEX_POINT('',#23852);
#7194=VERTEX_POINT('',#23854);
#7195=VERTEX_POINT('',#23857);
#7196=VERTEX_POINT('',#23862);
#8642=EDGE_CURVE('',#7193,#7193,#6168,.T.);
#8643=EDGE_CURVE('',#7194,#7194,#6169,.T.);
#8644=EDGE_CURVE('',#7195,#7195,#6170,.T.);
#8645=EDGE_CURVE('',#7195,#7193,#4777,.T.);
#8646=EDGE_CURVE('',#7194,#7196,#4778,.T.);
#8647=EDGE_CURVE('',#7196,#7196,#6171,.T.);
#11414=ORIENTED_EDGE('',*,*,#8642,.F.);
#11415=ORIENTED_EDGE('',*,*,#8643,.T.);
#11416=ORIENTED_EDGE('',*,*,#8644,.F.);
#11417=ORIENTED_EDGE('',*,*,#8645,.T.);
#11418=ORIENTED_EDGE('',*,*,#8642,.T.);
#11419=ORIENTED_EDGE('',*,*,#8645,.F.);
#11420=ORIENTED_EDGE('',*,*,#8644,.T.);
#11421=ORIENTED_EDGE('',*,*,#8643,.F.);
#11422=ORIENTED_EDGE('',*,*,#8646,.T.);
#11423=ORIENTED_EDGE('',*,*,#8647,.T.);
#11424=ORIENTED_EDGE('',*,*,#8646,.F.);
#11425=ORIENTED_EDGE('',*,*,#8647,.F.);
#12345=CYLINDRICAL_SURFACE('',#15946,0.350000000000001);
#12346=CYLINDRICAL_SURFACE('',#15949,0.199999999999999);
#13056=ADVANCED_FACE('',(#2689,#1570),#1983,.F.);
#13057=ADVANCED_FACE('',(#2690),#12345,.T.);
#13058=ADVANCED_FACE('',(#2691),#1984,.T.);
#13059=ADVANCED_FACE('',(#2692),#12346,.T.);
#13060=ADVANCED_FACE('',(#2693),#1985,.F.);
#13336=CLOSED_SHELL('',(#13056,#13057,#13058,#13059,#13060));
#15942=AXIS2_PLACEMENT_3D('',#23850,#19835,#19836);
#15943=AXIS2_PLACEMENT_3D('',#23851,#19837,#19838);
#15944=AXIS2_PLACEMENT_3D('',#23853,#19839,#19840);
#15945=AXIS2_PLACEMENT_3D('',#23855,#19841,#19842);
#15946=AXIS2_PLACEMENT_3D('',#23856,#19843,#19844);
#15947=AXIS2_PLACEMENT_3D('',#23858,#19845,#19846);
#15948=AXIS2_PLACEMENT_3D('',#23860,#19848,#19849);
#15949=AXIS2_PLACEMENT_3D('',#23861,#19850,#19851);
#15950=AXIS2_PLACEMENT_3D('',#23864,#19853,#19854);
#15951=AXIS2_PLACEMENT_3D('',#23865,#19855,#19856);
#19835=DIRECTION('axis',(0.,0.,1.));
#19836=DIRECTION('refdir',(1.,0.,0.));
#19837=DIRECTION('center_axis',(0.,1.,0.));
#19838=DIRECTION('ref_axis',(1.,0.,0.));
#19839=DIRECTION('center_axis',(0.,1.,0.));
#19840=DIRECTION('ref_axis',(1.,0.,0.));
#19841=DIRECTION('center_axis',(0.,1.,0.));
#19842=DIRECTION('ref_axis',(1.,0.,0.));
#19843=DIRECTION('center_axis',(0.,1.,0.));
#19844=DIRECTION('ref_axis',(1.,0.,0.));
#19845=DIRECTION('center_axis',(0.,1.,0.));
#19846=DIRECTION('ref_axis',(1.,0.,0.));
#19847=DIRECTION('',(0.,-1.,0.));
#19848=DIRECTION('center_axis',(0.,1.,0.));
#19849=DIRECTION('ref_axis',(1.,0.,0.));
#19850=DIRECTION('center_axis',(0.,1.,0.));
#19851=DIRECTION('ref_axis',(1.,0.,0.));
#19852=DIRECTION('',(0.,-1.,0.));
#19853=DIRECTION('center_axis',(0.,1.,0.));
#19854=DIRECTION('ref_axis',(1.,0.,0.));
#19855=DIRECTION('center_axis',(0.,1.,0.));
#19856=DIRECTION('ref_axis',(1.,0.,0.));
#23850=CARTESIAN_POINT('',(0.,0.,0.));
#23851=CARTESIAN_POINT('Origin',(20.6730642762322,-4.2,6.69185245480489));
#23852=CARTESIAN_POINT('',(20.3230642762322,-4.2,6.69185245480489));
#23853=CARTESIAN_POINT('Origin',(20.6730642762322,-4.2,6.69185245480489));
#23854=CARTESIAN_POINT('',(20.4730642762322,-4.2,6.69185245480489));
#23855=CARTESIAN_POINT('Origin',(20.6730642762322,-4.2,6.69185245480489));
#23856=CARTESIAN_POINT('Origin',(20.6730642762322,-4.2,6.69185245480489));
#23857=CARTESIAN_POINT('',(20.3230642762322,-4.1,6.69185245480489));
#23858=CARTESIAN_POINT('Origin',(20.6730642762322,-4.1,6.69185245480489));
#23859=CARTESIAN_POINT('',(20.3230642762322,-4.2,6.69185245480489));
#23860=CARTESIAN_POINT('Origin',(20.6730642762322,-4.1,6.69185245480489));
#23861=CARTESIAN_POINT('Origin',(20.6730642762322,-4.9,6.69185245480489));
#23862=CARTESIAN_POINT('',(20.4730642762322,-4.9,6.69185245480489));
#23863=CARTESIAN_POINT('',(20.4730642762322,-4.9,6.69185245480489));
#23864=CARTESIAN_POINT('Origin',(20.6730642762322,-4.9,6.69185245480489));
#23865=CARTESIAN_POINT('Origin',(20.6730642762322,-4.9,6.69185245480489));
#24952=UNCERTAINTY_MEASURE_WITH_UNIT(LENGTH_MEASURE(0.001),#25101,
'DISTANCE_ACCURACY_VALUE',
'Maximum model space distance between geometric entities at asserted c
onnectivities');
#24979=UNCERTAINTY_MEASURE_WITH_UNIT(LENGTH_MEASURE(0.001),#25101,
'DISTANCE_ACCURACY_VALUE',
'Maximum model space distance between geometric entities at asserted c
onnectivities');
#25073=(
GEOMETRIC_REPRESENTATION_CONTEXT(3)
GLOBAL_UNCERTAINTY_ASSIGNED_CONTEXT((#24952))
GLOBAL_UNIT_ASSIGNED_CONTEXT((#25101,#25103,#25104))
REPRESENTATION_CONTEXT('','3D')
);
#25100=(
GEOMETRIC_REPRESENTATION_CONTEXT(3)
GLOBAL_UNCERTAINTY_ASSIGNED_CONTEXT((#24979))
GLOBAL_UNIT_ASSIGNED_CONTEXT((#25101,#25103,#25104))
REPRESENTATION_CONTEXT('','3D')
);
#25101=(
LENGTH_UNIT()
NAMED_UNIT(*)
SI_UNIT(.CENTI.,.METRE.)
);
#25103=(
NAMED_UNIT(*)
PLANE_ANGLE_UNIT()
SI_UNIT($,.RADIAN.)
);
#25104=(
NAMED_UNIT(*)
SI_UNIT($,.STERADIAN.)
SOLID_ANGLE_UNIT()
);
#25198=SHAPE_DEFINITION_REPRESENTATION(#25392,#25603);
#25392=PRODUCT_DEFINITION_SHAPE('',$,#25724);
#25603=SHAPE_REPRESENTATION('',(#15942),#25073);
#25630=PRODUCT_DEFINITION_CONTEXT('part definition',#25992,'design');
#25724=PRODUCT_DEFINITION('M4 low-profile retaining screw (7)',
'M4 low-profile retaining screw (7)',#25844,#25630);
#25844=PRODUCT_DEFINITION_FORMATION('',$,#26087);
#25992=APPLICATION_CONTEXT(
'Core Data for Automotive Mechanical Design Process');
#25993=PRODUCT_CONTEXT('part definition',#25992,'mechanical');
#26087=PRODUCT('M4 low-profile retaining screw (7)',
'M4 low-profile retaining screw (7)','M4 low-profile retaining screw (7)',(#25993));
#26192=COLOUR_RGB('Black',0.12,0.14,0.17);
#26193=FILL_AREA_STYLE_COLOUR('',#26192);
#26194=FILL_AREA_STYLE('',(#26193));
#26195=SURFACE_STYLE_FILL_AREA(#26194);
#26196=SURFACE_SIDE_STYLE('',(#26195));
#26197=SURFACE_STYLE_USAGE(.BOTH.,#26196);
#26198=PRESENTATION_STYLE_ASSIGNMENT((#26197));
ENDSEC;
END-ISO-10303-21;
